ISO-10303-21;
HEADER;
/* Generated by software containing ST-Developer
 * from STEP Tools, Inc. (www.steptools.com) 
 */

FILE_DESCRIPTION(
/* description */ ('PAT-026'),
/* implementation_level */ '2;1');

FILE_NAME(
/* name */ 'M5x14 Cap Screw.step',
/* time_stamp */ '2026-10-28T22:25:58-07:00',
/* author */ (''),
/* organization */ (''),
/* preprocessor_version */ 'ST-DEVELOPER v20.2',
/* originating_system */ 'Autodesk Translation Framework v15.17.0.0',
/* authorisation */ '');

FILE_SCHEMA (('AUTOMOTIVE_DESIGN { 1 0 10303 214 3 1 1 }'));
ENDSEC;

DATA;
#10=MECHANICAL_DESIGN_GEOMETRIC_PRESENTATION_REPRESENTATION('',(#145),#12343);
#104=CONICAL_SURFACE('',#7565,0.4,0.785398163397448);
#105=CONICAL_SURFACE('',#7569,0.41,0.785398163397448);
#106=CONICAL_SURFACE('',#7573,0.26,0.463647609000806);
#115=ORIENTED_CLOSED_SHELL('',*,#7351,.F.);
#117=BREP_WITH_VOIDS('Body1',#7352,(#115));
#123=SHAPE_REPRESENTATION_RELATIONSHIP('SRR','None',#12400,#134);
#134=ADVANCED_BREP_SHAPE_REPRESENTATION('',(#117),#12335);
#145=STYLED_ITEM('',(#12540),#117);
#179=FACE_BOUND('',#1027,.T.);
#220=PLANE('',#7553);
#221=PLANE('',#7554);
#222=PLANE('',#7555);
#223=PLANE('',#7556);
#224=PLANE('',#7557);
#225=PLANE('',#7558);
#226=PLANE('',#7559);
#227=PLANE('',#7560);
#228=PLANE('',#7561);
#229=PLANE('',#7563);
#230=PLANE('',#7571);
#592=FACE_OUTER_BOUND('',#1013,.T.);
#593=FACE_OUTER_BOUND('',#1014,.T.);
#594=FACE_OUTER_BOUND('',#1015,.T.);
#595=FACE_OUTER_BOUND('',#1016,.T.);
#596=FACE_OUTER_BOUND('',#1017,.T.);
#597=FACE_OUTER_BOUND('',#1018,.T.);
#598=FACE_OUTER_BOUND('',#1019,.T.);
#599=FACE_OUTER_BOUND('',#1020,.T.);
#600=FACE_OUTER_BOUND('',#1021,.T.);
#601=FACE_OUTER_BOUND('',#1022,.T.);
#602=FACE_OUTER_BOUND('',#1023,.T.);
#603=FACE_OUTER_BOUND('',#1024,.T.);
#604=FACE_OUTER_BOUND('',#1025,.T.);
#605=FACE_OUTER_BOUND('',#1026,.T.);
#606=FACE_OUTER_BOUND('',#1028,.T.);
#607=FACE_OUTER_BOUND('',#1029,.T.);
#1013=EDGE_LOOP('',(#5085,#5086,#5087,#5088));
#1014=EDGE_LOOP('',(#5089,#5090,#5091,#5092));
#1015=EDGE_LOOP('',(#5093,#5094,#5095,#5096));
#1016=EDGE_LOOP('',(#5097,#5098,#5099,#5100));
#1017=EDGE_LOOP('',(#5101,#5102,#5103,#5104));
#1018=EDGE_LOOP('',(#5105,#5106,#5107,#5108));
#1019=EDGE_LOOP('',(#5109,#5110,#5111,#5112,#5113,#5114));
#1020=EDGE_LOOP('',(#5115,#5116,#5117,#5118,#5119,#5120));
#1021=EDGE_LOOP('',(#5121));
#1022=EDGE_LOOP('',(#5122));
#1023=EDGE_LOOP('',(#5123,#5124,#5125,#5126));
#1024=EDGE_LOOP('',(#5127,#5128,#5129,#5130));
#1025=EDGE_LOOP('',(#5131,#5132,#5133,#5134));
#1026=EDGE_LOOP('',(#5135));
#1027=EDGE_LOOP('',(#5136));
#1028=EDGE_LOOP('',(#5137,#5138,#5139,#5140));
#1029=EDGE_LOOP('',(#5141,#5142,#5143,#5144));
#1459=LINE('',#10243,#2331);
#1460=LINE('',#10245,#2332);
#1461=LINE('',#10247,#2333);
#1462=LINE('',#10248,#2334);
#1463=LINE('',#10251,#2335);
#1464=LINE('',#10253,#2336);
#1465=LINE('',#10254,#2337);
#1466=LINE('',#10257,#2338);
#1467=LINE('',#10259,#2339);
#1468=LINE('',#10260,#2340);
#1469=LINE('',#10263,#2341);
#1470=LINE('',#10265,#2342);
#1471=LINE('',#10266,#2343);
#1472=LINE('',#10269,#2344);
#1473=LINE('',#10271,#2345);
#1474=LINE('',#10272,#2346);
#1475=LINE('',#10274,#2347);
#1476=LINE('',#10275,#2348);
#1477=LINE('',#10287,#2349);
#1478=LINE('',#10291,#2350);
#1479=LINE('',#10295,#2351);
#1480=LINE('',#10302,#2352);
#1481=LINE('',#10304,#2353);
#2331=VECTOR('',#8255,1.);
#2332=VECTOR('',#8256,1.);
#2333=VECTOR('',#8257,1.);
#2334=VECTOR('',#8258,1.);
#2335=VECTOR('',#8261,1.);
#2336=VECTOR('',#8262,1.);
#2337=VECTOR('',#8263,1.);
#2338=VECTOR('',#8266,1.);
#2339=VECTOR('',#8267,1.);
#2340=VECTOR('',#8268,1.);
#2341=VECTOR('',#8271,1.);
#2342=VECTOR('',#8272,1.);
#2343=VECTOR('',#8273,1.);
#2344=VECTOR('',#8276,1.);
#2345=VECTOR('',#8277,1.);
#2346=VECTOR('',#8278,1.);
#2347=VECTOR('',#8281,1.);
#2348=VECTOR('',#8282,1.);
#2349=VECTOR('',#8299,0.4);
#2350=VECTOR('',#8304,0.425);
#2351=VECTOR('',#8309,0.41);
#2352=VECTOR('',#8318,0.26);
#2353=VECTOR('',#8321,0.25);
#3162=CIRCLE('',#7562,0.24505);
#3163=CIRCLE('',#7564,0.375);
#3164=CIRCLE('',#7566,0.425);
#3165=CIRCLE('',#7568,0.425);
#3166=CIRCLE('',#7570,0.395);
#3167=CIRCLE('',#7572,0.27);
#3168=CIRCLE('',#7574,0.24505);
#3323=VERTEX_POINT('',#10241);
#3324=VERTEX_POINT('',#10242);
#3325=VERTEX_POINT('',#10244);
#3326=VERTEX_POINT('',#10246);
#3327=VERTEX_POINT('',#10250);
#3328=VERTEX_POINT('',#10252);
#3329=VERTEX_POINT('',#10256);
#3330=VERTEX_POINT('',#10258);
#3331=VERTEX_POINT('',#10262);
#3332=VERTEX_POINT('',#10264);
#3333=VERTEX_POINT('',#10268);
#3334=VERTEX_POINT('',#10270);
#3335=VERTEX_POINT('',#10279);
#3336=VERTEX_POINT('',#10282);
#3337=VERTEX_POINT('',#10285);
#3338=VERTEX_POINT('',#10289);
#3339=VERTEX_POINT('',#10293);
#3340=VERTEX_POINT('',#10297);
#3341=VERTEX_POINT('',#10300);
#3986=EDGE_CURVE('',#3323,#3324,#1459,.T.);
#3987=EDGE_CURVE('',#3324,#3325,#1460,.T.);
#3988=EDGE_CURVE('',#3325,#3326,#1461,.T.);
#3989=EDGE_CURVE('',#3323,#3326,#1462,.T.);
#3990=EDGE_CURVE('',#3324,#3327,#1463,.T.);
#3991=EDGE_CURVE('',#3327,#3328,#1464,.T.);
#3992=EDGE_CURVE('',#3328,#3325,#1465,.T.);
#3993=EDGE_CURVE('',#3327,#3329,#1466,.T.);
#3994=EDGE_CURVE('',#3329,#3330,#1467,.T.);
#3995=EDGE_CURVE('',#3330,#3328,#1468,.T.);
#3996=EDGE_CURVE('',#3329,#3331,#1469,.T.);
#3997=EDGE_CURVE('',#3331,#3332,#1470,.T.);
#3998=EDGE_CURVE('',#3332,#3330,#1471,.T.);
#3999=EDGE_CURVE('',#3331,#3333,#1472,.T.);
#4000=EDGE_CURVE('',#3333,#3334,#1473,.T.);
#4001=EDGE_CURVE('',#3334,#3332,#1474,.T.);
#4002=EDGE_CURVE('',#3333,#3323,#1475,.T.);
#4003=EDGE_CURVE('',#3326,#3334,#1476,.T.);
#4004=EDGE_CURVE('',#3335,#3335,#3162,.T.);
#4005=EDGE_CURVE('',#3336,#3336,#3163,.T.);
#4006=EDGE_CURVE('',#3337,#3337,#3164,.T.);
#4007=EDGE_CURVE('',#3337,#3336,#1477,.T.);
#4008=EDGE_CURVE('',#3338,#3338,#3165,.T.);
#4009=EDGE_CURVE('',#3338,#3337,#1478,.T.);
#4010=EDGE_CURVE('',#3339,#3339,#3166,.T.);
#4011=EDGE_CURVE('',#3339,#3338,#1479,.T.);
#4012=EDGE_CURVE('',#3340,#3340,#3167,.T.);
#4013=EDGE_CURVE('',#3341,#3341,#3168,.F.);
#4014=EDGE_CURVE('',#3341,#3340,#1480,.T.);
#4015=EDGE_CURVE('',#3335,#3341,#1481,.T.);
#5085=ORIENTED_EDGE('',*,*,#3986,.T.);
#5086=ORIENTED_EDGE('',*,*,#3987,.T.);
#5087=ORIENTED_EDGE('',*,*,#3988,.T.);
#5088=ORIENTED_EDGE('',*,*,#3989,.F.);
#5089=ORIENTED_EDGE('',*,*,#3990,.T.);
#5090=ORIENTED_EDGE('',*,*,#3991,.T.);
#5091=ORIENTED_EDGE('',*,*,#3992,.T.);
#5092=ORIENTED_EDGE('',*,*,#3987,.F.);
#5093=ORIENTED_EDGE('',*,*,#3993,.T.);
#5094=ORIENTED_EDGE('',*,*,#3994,.T.);
#5095=ORIENTED_EDGE('',*,*,#3995,.T.);
#5096=ORIENTED_EDGE('',*,*,#3991,.F.);
#5097=ORIENTED_EDGE('',*,*,#3996,.T.);
#5098=ORIENTED_EDGE('',*,*,#3997,.T.);
#5099=ORIENTED_EDGE('',*,*,#3998,.T.);
#5100=ORIENTED_EDGE('',*,*,#3994,.F.);
#5101=ORIENTED_EDGE('',*,*,#3999,.T.);
#5102=ORIENTED_EDGE('',*,*,#4000,.T.);
#5103=ORIENTED_EDGE('',*,*,#4001,.T.);
#5104=ORIENTED_EDGE('',*,*,#3997,.F.);
#5105=ORIENTED_EDGE('',*,*,#4002,.T.);
#5106=ORIENTED_EDGE('',*,*,#3989,.T.);
#5107=ORIENTED_EDGE('',*,*,#4003,.T.);
#5108=ORIENTED_EDGE('',*,*,#4000,.F.);
#5109=ORIENTED_EDGE('',*,*,#4002,.F.);
#5110=ORIENTED_EDGE('',*,*,#3999,.F.);
#5111=ORIENTED_EDGE('',*,*,#3996,.F.);
#5112=ORIENTED_EDGE('',*,*,#3993,.F.);
#5113=ORIENTED_EDGE('',*,*,#3990,.F.);
#5114=ORIENTED_EDGE('',*,*,#3986,.F.);
#5115=ORIENTED_EDGE('',*,*,#4003,.F.);
#5116=ORIENTED_EDGE('',*,*,#3988,.F.);
#5117=ORIENTED_EDGE('',*,*,#3992,.F.);
#5118=ORIENTED_EDGE('',*,*,#3995,.F.);
#5119=ORIENTED_EDGE('',*,*,#3998,.F.);
#5120=ORIENTED_EDGE('',*,*,#4001,.F.);
#5121=ORIENTED_EDGE('',*,*,#4004,.F.);
#5122=ORIENTED_EDGE('',*,*,#4005,.F.);
#5123=ORIENTED_EDGE('',*,*,#4006,.F.);
#5124=ORIENTED_EDGE('',*,*,#4007,.T.);
#5125=ORIENTED_EDGE('',*,*,#4005,.T.);
#5126=ORIENTED_EDGE('',*,*,#4007,.F.);
#5127=ORIENTED_EDGE('',*,*,#4008,.F.);
#5128=ORIENTED_EDGE('',*,*,#4009,.T.);
#5129=ORIENTED_EDGE('',*,*,#4006,.T.);
#5130=ORIENTED_EDGE('',*,*,#4009,.F.);
#5131=ORIENTED_EDGE('',*,*,#4010,.F.);
#5132=ORIENTED_EDGE('',*,*,#4011,.T.);
#5133=ORIENTED_EDGE('',*,*,#4008,.T.);
#5134=ORIENTED_EDGE('',*,*,#4011,.F.);
#5135=ORIENTED_EDGE('',*,*,#4010,.T.);
#5136=ORIENTED_EDGE('',*,*,#4012,.F.);
#5137=ORIENTED_EDGE('',*,*,#4013,.F.);
#5138=ORIENTED_EDGE('',*,*,#4014,.T.);
#5139=ORIENTED_EDGE('',*,*,#4012,.T.);
#5140=ORIENTED_EDGE('',*,*,#4014,.F.);
#5141=ORIENTED_EDGE('',*,*,#4004,.T.);
#5142=ORIENTED_EDGE('',*,*,#4015,.T.);
#5143=ORIENTED_EDGE('',*,*,#4013,.T.);
#5144=ORIENTED_EDGE('',*,*,#4015,.F.);
#6924=CYLINDRICAL_SURFACE('',#7567,0.425);
#6925=CYLINDRICAL_SURFACE('',#7575,0.24505);
#6983=ADVANCED_FACE('',(#592),#220,.F.);
#6984=ADVANCED_FACE('',(#593),#221,.F.);
#6985=ADVANCED_FACE('',(#594),#222,.F.);
#6986=ADVANCED_FACE('',(#595),#223,.F.);
#6987=ADVANCED_FACE('',(#596),#224,.F.);
#6988=ADVANCED_FACE('',(#597),#225,.F.);
#6989=ADVANCED_FACE('',(#598),#226,.F.);
#6990=ADVANCED_FACE('',(#599),#227,.F.);
#6991=ADVANCED_FACE('',(#600),#228,.F.);
#6992=ADVANCED_FACE('',(#601),#229,.T.);
#6993=ADVANCED_FACE('',(#602),#104,.T.);
#6994=ADVANCED_FACE('',(#603),#6924,.T.);
#6995=ADVANCED_FACE('',(#604),#105,.T.);
#6996=ADVANCED_FACE('',(#605,#179),#230,.T.);
#6997=ADVANCED_FACE('',(#606),#106,.T.);
#6998=ADVANCED_FACE('',(#607),#6925,.T.);
#7351=CLOSED_SHELL('',(#6983,#6984,#6985,#6986,#6987,#6988,#6989,#6990));
#7352=CLOSED_SHELL('',(#6991,#6992,#6993,#6994,#6995,#6996,#6997,#6998));
#7552=AXIS2_PLACEMENT_3D('',#10239,#8251,#8252);
#7553=AXIS2_PLACEMENT_3D('',#10240,#8253,#8254);
#7554=AXIS2_PLACEMENT_3D('',#10249,#8259,#8260);
#7555=AXIS2_PLACEMENT_3D('',#10255,#8264,#8265);
#7556=AXIS2_PLACEMENT_3D('',#10261,#8269,#8270);
#7557=AXIS2_PLACEMENT_3D('',#10267,#8274,#8275);
#7558=AXIS2_PLACEMENT_3D('',#10273,#8279,#8280);
#7559=AXIS2_PLACEMENT_3D('',#10276,#8283,#8284);
#7560=AXIS2_PLACEMENT_3D('',#10277,#8285,#8286);
#7561=AXIS2_PLACEMENT_3D('',#10278,#8287,#8288);
#7562=AXIS2_PLACEMENT_3D('',#10280,#8289,#8290);
#7563=AXIS2_PLACEMENT_3D('',#10281,#8291,#8292);
#7564=AXIS2_PLACEMENT_3D('',#10283,#8293,#8294);
#7565=AXIS2_PLACEMENT_3D('',#10284,#8295,#8296);
#7566=AXIS2_PLACEMENT_3D('',#10286,#8297,#8298);
#7567=AXIS2_PLACEMENT_3D('',#10288,#8300,#8301);
#7568=AXIS2_PLACEMENT_3D('',#10290,#8302,#8303);
#7569=AXIS2_PLACEMENT_3D('',#10292,#8305,#8306);
#7570=AXIS2_PLACEMENT_3D('',#10294,#8307,#8308);
#7571=AXIS2_PLACEMENT_3D('',#10296,#8310,#8311);
#7572=AXIS2_PLACEMENT_3D('',#10298,#8312,#8313);
#7573=AXIS2_PLACEMENT_3D('',#10299,#8314,#8315);
#7574=AXIS2_PLACEMENT_3D('',#10301,#8316,#8317);
#7575=AXIS2_PLACEMENT_3D('',#10303,#8319,#8320);
#8251=DIRECTION('axis',(0.,0.,1.));
#8252=DIRECTION('refdir',(1.,0.,0.));
#8253=DIRECTION('center_axis',(0.866025403784439,0.,-0.5));
#8254=DIRECTION('ref_axis',(0.5,0.,0.866025403784439));
#8255=DIRECTION('',(-0.5,0.,-0.866025403784439));
#8256=DIRECTION('',(0.,-1.,0.));
#8257=DIRECTION('',(0.5,0.,0.866025403784439));
#8258=DIRECTION('',(0.,-1.,0.));
#8259=DIRECTION('center_axis',(1.20185167898973E-16,0.,-1.));
#8260=DIRECTION('ref_axis',(1.,0.,1.20185167898973E-16));
#8261=DIRECTION('',(-1.,0.,-1.20185167898973E-16));
#8262=DIRECTION('',(0.,-1.,0.));
#8263=DIRECTION('',(1.,0.,1.20185167898973E-16));
#8264=DIRECTION('center_axis',(-0.866025403784439,0.,-0.5));
#8265=DIRECTION('ref_axis',(0.5,0.,-0.866025403784439));
#8266=DIRECTION('',(-0.5,0.,0.866025403784439));
#8267=DIRECTION('',(0.,-1.,0.));
#8268=DIRECTION('',(0.5,0.,-0.866025403784439));
#8269=DIRECTION('center_axis',(-0.866025403784439,0.,0.5));
#8270=DIRECTION('ref_axis',(-0.5,0.,-0.866025403784439));
#8271=DIRECTION('',(0.5,0.,0.866025403784439));
#8272=DIRECTION('',(0.,-1.,0.));
#8273=DIRECTION('',(-0.5,0.,-0.866025403784439));
#8274=DIRECTION('center_axis',(-2.40370335797945E-16,0.,1.));
#8275=DIRECTION('ref_axis',(-1.,0.,-2.40370335797945E-16));
#8276=DIRECTION('',(1.,0.,2.40370335797945E-16));
#8277=DIRECTION('',(0.,-1.,0.));
#8278=DIRECTION('',(-1.,0.,-2.40370335797945E-16));
#8279=DIRECTION('center_axis',(0.866025403784439,0.,0.5));
#8280=DIRECTION('ref_axis',(-0.5,0.,0.866025403784439));
#8281=DIRECTION('',(0.5,0.,-0.866025403784439));
#8282=DIRECTION('',(-0.5,0.,0.866025403784439));
#8283=DIRECTION('center_axis',(0.,1.,0.));
#8284=DIRECTION('ref_axis',(1.,0.,0.));
#8285=DIRECTION('center_axis',(0.,-1.,0.));
#8286=DIRECTION('ref_axis',(0.,0.,-1.));
#8287=DIRECTION('center_axis',(0.,1.,0.));
#8288=DIRECTION('ref_axis',(1.,0.,0.));
#8289=DIRECTION('center_axis',(0.,1.,0.));
#8290=DIRECTION('ref_axis',(1.,0.,0.));
#8291=DIRECTION('center_axis',(0.,1.,0.));
#8292=DIRECTION('ref_axis',(0.,0.,1.));
#8293=DIRECTION('center_axis',(0.,-1.,0.));
#8294=DIRECTION('ref_axis',(1.,0.,0.));
#8295=DIRECTION('center_axis',(0.,-1.,0.));
#8296=DIRECTION('ref_axis',(1.,0.,0.));
#8297=DIRECTION('center_axis',(0.,-1.,0.));
#8298=DIRECTION('ref_axis',(1.,0.,0.));
#8299=DIRECTION('',(0.707106781186548,0.707106781186547,8.65956056235493E-17));
#8300=DIRECTION('center_axis',(0.,-1.,0.));
#8301=DIRECTION('ref_axis',(1.,0.,0.));
#8302=DIRECTION('center_axis',(0.,-1.,0.));
#8303=DIRECTION('ref_axis',(1.,0.,0.));
#8304=DIRECTION('',(0.,1.,0.));
#8305=DIRECTION('center_axis',(0.,1.,0.));
#8306=DIRECTION('ref_axis',(1.,0.,0.));
#8307=DIRECTION('center_axis',(0.,-1.,0.));
#8308=DIRECTION('ref_axis',(1.,0.,0.));
#8309=DIRECTION('',(-0.707106781186547,0.707106781186548,-8.65956056235493E-17));
#8310=DIRECTION('center_axis',(0.,-1.,0.));
#8311=DIRECTION('ref_axis',(0.,0.,-1.));
#8312=DIRECTION('center_axis',(0.,-1.,0.));
#8313=DIRECTION('ref_axis',(1.,0.,0.));
#8314=DIRECTION('center_axis',(0.,1.,0.));
#8315=DIRECTION('ref_axis',(1.,0.,0.));
#8316=DIRECTION('center_axis',(0.,1.,0.));
#8317=DIRECTION('ref_axis',(1.,0.,0.));
#8318=DIRECTION('',(-0.447213595499958,0.894427190999916,-5.47678698264203E-17));
#8319=DIRECTION('center_axis',(0.,-1.,0.));
#8320=DIRECTION('ref_axis',(1.,0.,0.));
#8321=DIRECTION('',(0.,1.,0.));
#10239=CARTESIAN_POINT('',(0.,0.,0.));
#10240=CARTESIAN_POINT('Origin',(0.115470053837925,-0.5,-0.2));
#10241=CARTESIAN_POINT('',(0.23094010767585,-0.5,0.));
#10242=CARTESIAN_POINT('',(0.115470053837925,-0.5,-0.2));
#10243=CARTESIAN_POINT('',(0.23094010767585,-0.5,0.));
#10244=CARTESIAN_POINT('',(0.115470053837925,-0.8,-0.2));
#10245=CARTESIAN_POINT('',(0.115470053837925,-0.5,-0.2));
#10246=CARTESIAN_POINT('',(0.23094010767585,-0.8,0.));
#10247=CARTESIAN_POINT('',(0.23094010767585,-0.8,0.));
#10248=CARTESIAN_POINT('',(0.23094010767585,-0.5,0.));
#10249=CARTESIAN_POINT('Origin',(-0.115470053837925,-0.5,-0.2));
#10250=CARTESIAN_POINT('',(-0.115470053837925,-0.5,-0.2));
#10251=CARTESIAN_POINT('',(0.115470053837925,-0.5,-0.2));
#10252=CARTESIAN_POINT('',(-0.115470053837925,-0.8,-0.2));
#10253=CARTESIAN_POINT('',(-0.115470053837925,-0.5,-0.2));
#10254=CARTESIAN_POINT('',(0.115470053837925,-0.8,-0.2));
#10255=CARTESIAN_POINT('Origin',(-0.23094010767585,-0.5,-2.77555756156289E-17));
#10256=CARTESIAN_POINT('',(-0.23094010767585,-0.5,-2.82820063659975E-17));
#10257=CARTESIAN_POINT('',(-0.115470053837925,-0.5,-0.2));
#10258=CARTESIAN_POINT('',(-0.23094010767585,-0.8,-2.77555756156289E-17));
#10259=CARTESIAN_POINT('',(-0.23094010767585,-0.5,-2.82820063659975E-17));
#10260=CARTESIAN_POINT('',(-0.115470053837925,-0.8,-0.2));
#10261=CARTESIAN_POINT('Origin',(-0.115470053837925,-0.5,0.2));
#10262=CARTESIAN_POINT('',(-0.115470053837925,-0.5,0.2));
#10263=CARTESIAN_POINT('',(-0.23094010767585,-0.5,-2.82820063659975E-17));
#10264=CARTESIAN_POINT('',(-0.115470053837925,-0.8,0.2));
#10265=CARTESIAN_POINT('',(-0.115470053837925,-0.5,0.2));
#10266=CARTESIAN_POINT('',(-0.23094010767585,-0.8,-2.82820063659975E-17));
#10267=CARTESIAN_POINT('Origin',(0.115470053837925,-0.5,0.2));
#10268=CARTESIAN_POINT('',(0.115470053837925,-0.5,0.2));
#10269=CARTESIAN_POINT('',(-0.115470053837925,-0.5,0.2));
#10270=CARTESIAN_POINT('',(0.115470053837925,-0.8,0.2));
#10271=CARTESIAN_POINT('',(0.115470053837925,-0.5,0.2));
#10272=CARTESIAN_POINT('',(-0.115470053837925,-0.8,0.2));
#10273=CARTESIAN_POINT('Origin',(0.23094010767585,-0.5,0.));
#10274=CARTESIAN_POINT('',(0.115470053837925,-0.5,0.2));
#10275=CARTESIAN_POINT('',(0.115470053837925,-0.8,0.2));
#10276=CARTESIAN_POINT('Origin',(0.,-0.5,0.));
#10277=CARTESIAN_POINT('Origin',(0.,-0.8,0.));
#10278=CARTESIAN_POINT('Origin',(0.,-1.4,0.));
#10279=CARTESIAN_POINT('',(-0.24505,-1.4,3.00099698131059E-17));
#10280=CARTESIAN_POINT('Origin',(0.,-1.4,0.));
#10281=CARTESIAN_POINT('Origin',(0.375,0.5,0.));
#10282=CARTESIAN_POINT('',(-0.375,0.5,-4.59242549680257E-17));
#10283=CARTESIAN_POINT('Origin',(0.,0.5,0.));
#10284=CARTESIAN_POINT('Origin',(0.,0.475,0.));
#10285=CARTESIAN_POINT('',(-0.425,0.45,-5.20474889637625E-17));
#10286=CARTESIAN_POINT('Origin',(0.,0.45,0.));
#10287=CARTESIAN_POINT('',(-0.4,0.475,-4.89858719658941E-17));
#10288=CARTESIAN_POINT('Origin',(0.,0.24,0.));
#10289=CARTESIAN_POINT('',(-0.425,0.0299999999999998,-5.20474889637625E-17));
#10290=CARTESIAN_POINT('Origin',(0.,0.0299999999999998,0.));
#10291=CARTESIAN_POINT('',(-0.425,0.24,-5.20474889637625E-17));
#10292=CARTESIAN_POINT('Origin',(0.,0.0150000000000001,0.));
#10293=CARTESIAN_POINT('',(-0.395,4.85722573273506E-17,-4.83735485663204E-17));
#10294=CARTESIAN_POINT('Origin',(0.,0.,0.));
#10295=CARTESIAN_POINT('',(-0.41,0.0150000000000001,-5.02105187650415E-17));
#10296=CARTESIAN_POINT('Origin',(0.27,0.,0.));
#10297=CARTESIAN_POINT('',(-0.27,0.,-3.30654635769785E-17));
#10298=CARTESIAN_POINT('Origin',(0.,0.,0.));
#10299=CARTESIAN_POINT('Origin',(0.,-0.02,0.));
#10300=CARTESIAN_POINT('',(-0.24505,-0.0498999999999999,3.00099698131059E-17));
#10301=CARTESIAN_POINT('Origin',(0.,-0.0498999999999999,0.));
#10302=CARTESIAN_POINT('',(-0.26,-0.02,-3.18408167778312E-17));
#10303=CARTESIAN_POINT('Origin',(0.,-0.995,0.));
#10304=CARTESIAN_POINT('',(-0.24505,-0.995,-3.00099698131059E-17));
#12321=UNCERTAINTY_MEASURE_WITH_UNIT(LENGTH_MEASURE(0.001),#12344,
'DISTANCE_ACCURACY_VALUE',
'Maximum model space distance between geometric entities at asserted c
onnectivities');
#12329=UNCERTAINTY_MEASURE_WITH_UNIT(LENGTH_MEASURE(0.001),#12344,
'DISTANCE_ACCURACY_VALUE',
'Maximum model space distance between geometric entities at asserted c
onnectivities');
#12335=(
GEOMETRIC_REPRESENTATION_CONTEXT(3)
GLOBAL_UNCERTAINTY_ASSIGNED_CONTEXT((#12321))
GLOBAL_UNIT_ASSIGNED_CONTEXT((#12344,#12346,#12347))
REPRESENTATION_CONTEXT('','3D')
);
#12343=(
GEOMETRIC_REPRESENTATION_CONTEXT(3)
GLOBAL_UNCERTAINTY_ASSIGNED_CONTEXT((#12329))
GLOBAL_UNIT_ASSIGNED_CONTEXT((#12344,#12346,#12347))
REPRESENTATION_CONTEXT('','3D')
);
#12344=(
LENGTH_UNIT()
NAMED_UNIT(*)
SI_UNIT(.CENTI.,.METRE.)
);
#12346=(
NAMED_UNIT(*)
PLANE_ANGLE_UNIT()
SI_UNIT($,.RADIAN.)
);
#12347=(
NAMED_UNIT(*)
SI_UNIT($,.STERADIAN.)
SOLID_ANGLE_UNIT()
);
#12353=SHAPE_DEFINITION_REPRESENTATION(#12366,#12400);
#12366=PRODUCT_DEFINITION_SHAPE('',$,#12414);
#12400=SHAPE_REPRESENTATION('',(#7552),#12335);
#12408=PRODUCT_DEFINITION_CONTEXT('part definition',#12449,'design');
#12414=PRODUCT_DEFINITION('M5x14 Cap Screw','M5x14 Cap Screw',#12427,
#12408);
#12427=PRODUCT_DEFINITION_FORMATION('',$,#12456);
#12449=APPLICATION_CONTEXT(
'Core Data for Automotive Mechanical Design Process');
#12450=PRODUCT_CONTEXT('part definition',#12449,'mechanical');
#12456=PRODUCT('M5x14 Cap Screw','M5x14 Cap Screw',
'M5x14 Cap Screw',(#12450));
#12534=COLOUR_RGB('Black',0.12,0.14,0.17);
#12535=FILL_AREA_STYLE_COLOUR('',#12534);
#12536=FILL_AREA_STYLE('',(#12535));
#12537=SURFACE_STYLE_FILL_AREA(#12536);
#12538=SURFACE_SIDE_STYLE('',(#12537));
#12539=SURFACE_STYLE_USAGE(.BOTH.,#12538);
#12540=PRESENTATION_STYLE_ASSIGNMENT((#12539));
ENDSEC;
END-ISO-10303-21;
